ISO-10303-21;
HEADER;
/* Generated by software containing ST-Developer
 * from STEP Tools, Inc. (www.steptools.com) 
 */

FILE_DESCRIPTION(
/* description */ ('Four-bar parallelogram arm'),
/* implementation_level */ '2;1');

FILE_NAME(
/* name */ 'Pivot keeper (2).step',
/* time_stamp */ '2026-10-28T03:24:55-07:00',
/* author */ (''),
/* organization */ (''),
/* preprocessor_version */ 'ST-DEVELOPER v20.2',
/* originating_system */ 'Autodesk Translation Framework v15.17.0.0',
/* authorisation */ '');

FILE_SCHEMA (('AUTOMOTIVE_DESIGN { 1 0 10303 214 3 1 1 }'));
ENDSEC;

DATA;
#10=MECHANICAL_DESIGN_GEOMETRIC_PRESENTATION_REPRESENTATION('',(#673),#14512);
#565=SHAPE_REPRESENTATION_RELATIONSHIP('SRR','None',#14790,#615);
#615=ADVANCED_BREP_SHAPE_REPRESENTATION('',(#729),#14505);
#673=STYLED_ITEM('',(#15101),#729);
#729=MANIFOLD_SOLID_BREP('Body1',#7379);
#986=FACE_BOUND('',#2246,.T.);
#987=FACE_BOUND('',#2248,.T.);
#1175=PLANE('',#8827);
#1176=PLANE('',#8828);
#1572=FACE_OUTER_BOUND('',#2243,.T.);
#1573=FACE_OUTER_BOUND('',#2244,.T.);
#1574=FACE_OUTER_BOUND('',#2245,.T.);
#1575=FACE_OUTER_BOUND('',#2247,.T.);
#2243=EDGE_LOOP('',(#6548,#6549,#6550,#6551));
#2244=EDGE_LOOP('',(#6552,#6553,#6554,#6555));
#2245=EDGE_LOOP('',(#6556));
#2246=EDGE_LOOP('',(#6557));
#2247=EDGE_LOOP('',(#6558));
#2248=EDGE_LOOP('',(#6559));
#2665=LINE('',#14159,#3059);
#2666=LINE('',#14165,#3060);
#3059=VECTOR('',#11093,0.225000000000001);
#3060=VECTOR('',#11100,0.899999999999999);
#3503=CIRCLE('',#8822,0.225000000000001);
#3504=CIRCLE('',#8823,0.225000000000001);
#3505=CIRCLE('',#8825,0.899999999999999);
#3506=CIRCLE('',#8826,0.899999999999999);
#4071=VERTEX_POINT('',#14156);
#4072=VERTEX_POINT('',#14158);
#4073=VERTEX_POINT('',#14162);
#4074=VERTEX_POINT('',#14164);
#4905=EDGE_CURVE('',#4071,#4071,#3503,.T.);
#4906=EDGE_CURVE('',#4071,#4072,#2665,.T.);
#4907=EDGE_CURVE('',#4072,#4072,#3504,.T.);
#4908=EDGE_CURVE('',#4073,#4073,#3505,.T.);
#4909=EDGE_CURVE('',#4073,#4074,#2666,.T.);
#4910=EDGE_CURVE('',#4074,#4074,#3506,.T.);
#6548=ORIENTED_EDGE('',*,*,#4905,.F.);
#6549=ORIENTED_EDGE('',*,*,#4906,.T.);
#6550=ORIENTED_EDGE('',*,*,#4907,.T.);
#6551=ORIENTED_EDGE('',*,*,#4906,.F.);
#6552=ORIENTED_EDGE('',*,*,#4908,.F.);
#6553=ORIENTED_EDGE('',*,*,#4909,.T.);
#6554=ORIENTED_EDGE('',*,*,#4910,.T.);
#6555=ORIENTED_EDGE('',*,*,#4909,.F.);
#6556=ORIENTED_EDGE('',*,*,#4908,.T.);
#6557=ORIENTED_EDGE('',*,*,#4905,.T.);
#6558=ORIENTED_EDGE('',*,*,#4910,.F.);
#6559=ORIENTED_EDGE('',*,*,#4907,.F.);
#6887=CYLINDRICAL_SURFACE('',#8821,0.225000000000001);
#6888=CYLINDRICAL_SURFACE('',#8824,0.899999999999999);
#7277=ADVANCED_FACE('',(#1572),#6887,.F.);
#7278=ADVANCED_FACE('',(#1573),#6888,.T.);
#7279=ADVANCED_FACE('',(#1574,#986),#1175,.T.);
#7280=ADVANCED_FACE('',(#1575,#987),#1176,.F.);
#7379=CLOSED_SHELL('',(#7277,#7278,#7279,#7280));
#8820=AXIS2_PLACEMENT_3D('',#14154,#11087,#11088);
#8821=AXIS2_PLACEMENT_3D('',#14155,#11089,#11090);
#8822=AXIS2_PLACEMENT_3D('',#14157,#11091,#11092);
#8823=AXIS2_PLACEMENT_3D('',#14160,#11094,#11095);
#8824=AXIS2_PLACEMENT_3D('',#14161,#11096,#11097);
#8825=AXIS2_PLACEMENT_3D('',#14163,#11098,#11099);
#8826=AXIS2_PLACEMENT_3D('',#14166,#11101,#11102);
#8827=AXIS2_PLACEMENT_3D('',#14167,#11103,#11104);
#8828=AXIS2_PLACEMENT_3D('',#14168,#11105,#11106);
#11087=DIRECTION('axis',(0.,0.,1.));
#11088=DIRECTION('refdir',(1.,0.,0.));
#11089=DIRECTION('center_axis',(0.,1.,0.));
#11090=DIRECTION('ref_axis',(1.,0.,0.));
#11091=DIRECTION('center_axis',(0.,-1.,0.));
#11092=DIRECTION('ref_axis',(1.,0.,0.));
#11093=DIRECTION('',(0.,-1.,0.));
#11094=DIRECTION('center_axis',(0.,-1.,0.));
#11095=DIRECTION('ref_axis',(1.,0.,0.));
#11096=DIRECTION('center_axis',(0.,1.,0.));
#11097=DIRECTION('ref_axis',(1.,0.,0.));
#11098=DIRECTION('center_axis',(0.,1.,0.));
#11099=DIRECTION('ref_axis',(1.,0.,0.));
#11100=DIRECTION('',(0.,-1.,0.));
#11101=DIRECTION('center_axis',(0.,1.,0.));
#11102=DIRECTION('ref_axis',(1.,0.,0.));
#11103=DIRECTION('center_axis',(0.,1.,0.));
#11104=DIRECTION('ref_axis',(1.,0.,0.));
#11105=DIRECTION('center_axis',(0.,1.,0.));
#11106=DIRECTION('ref_axis',(1.,0.,0.));
#14154=CARTESIAN_POINT('',(0.,0.,0.));
#14155=CARTESIAN_POINT('Origin',(20.,-1.8,8.));
#14156=CARTESIAN_POINT('',(19.775,-1.6,8.));
#14157=CARTESIAN_POINT('Origin',(20.,-1.6,8.));
#14158=CARTESIAN_POINT('',(19.775,-1.8,8.));
#14159=CARTESIAN_POINT('',(19.775,-1.8,8.));
#14160=CARTESIAN_POINT('Origin',(20.,-1.8,8.));
#14161=CARTESIAN_POINT('Origin',(20.,-1.8,8.));
#14162=CARTESIAN_POINT('',(19.1,-1.6,8.));
#14163=CARTESIAN_POINT('Origin',(20.,-1.6,8.));
#14164=CARTESIAN_POINT('',(19.1,-1.8,8.));
#14165=CARTESIAN_POINT('',(19.1,-1.8,8.));
#14166=CARTESIAN_POINT('Origin',(20.,-1.8,8.));
#14167=CARTESIAN_POINT('Origin',(20.,-1.6,8.));
#14168=CARTESIAN_POINT('Origin',(20.,-1.8,8.));
#14448=UNCERTAINTY_MEASURE_WITH_UNIT(LENGTH_MEASURE(0.001),#14513,
'DISTANCE_ACCURACY_VALUE',
'Maximum model space distance between geometric entities at asserted c
onnectivities');
#14455=UNCERTAINTY_MEASURE_WITH_UNIT(LENGTH_MEASURE(0.001),#14513,
'DISTANCE_ACCURACY_VALUE',
'Maximum model space distance between geometric entities at asserted c
onnectivities');
#14505=(
GEOMETRIC_REPRESENTATION_CONTEXT(3)
GLOBAL_UNCERTAINTY_ASSIGNED_CONTEXT((#14448))
GLOBAL_UNIT_ASSIGNED_CONTEXT((#14513,#14515,#14516))
REPRESENTATION_CONTEXT('','3D')
);
#14512=(
GEOMETRIC_REPRESENTATION_CONTEXT(3)
GLOBAL_UNCERTAINTY_ASSIGNED_CONTEXT((#14455))
GLOBAL_UNIT_ASSIGNED_CONTEXT((#14513,#14515,#14516))
REPRESENTATION_CONTEXT('','3D')
);
#14513=(
LENGTH_UNIT()
NAMED_UNIT(*)
SI_UNIT(.CENTI.,.METRE.)
);
#14515=(
NAMED_UNIT(*)
PLANE_ANGLE_UNIT()
SI_UNIT($,.RADIAN.)
);
#14516=(
NAMED_UNIT(*)
SI_UNIT($,.STERADIAN.)
SOLID_ANGLE_UNIT()
);
#14566=SHAPE_DEFINITION_REPRESENTATION(#14682,#14790);
#14682=PRODUCT_DEFINITION_SHAPE('',$,#14847);
#14790=SHAPE_REPRESENTATION('',(#8820),#14505);
#14797=PRODUCT_DEFINITION_CONTEXT('part definition',#14967,'design');
#14847=PRODUCT_DEFINITION('Pivot keeper (2)','Pivot keeper (2)',#14903,#14797);
#14903=PRODUCT_DEFINITION_FORMATION('',$,#15018);
#14967=APPLICATION_CONTEXT(
'Core Data for Automotive Mechanical Design Process');
#14968=PRODUCT_CONTEXT('part definition',#14967,'mechanical');
#15018=PRODUCT('Pivot keeper (2)','Pivot keeper (2)','Pivot keeper (2)',(#14968));
#15095=COLOUR_RGB('Off White',0.89,0.88,0.83);
#15096=FILL_AREA_STYLE_COLOUR('',#15095);
#15097=FILL_AREA_STYLE('',(#15096));
#15098=SURFACE_STYLE_FILL_AREA(#15097);
#15099=SURFACE_SIDE_STYLE('',(#15098));
#15100=SURFACE_STYLE_USAGE(.BOTH.,#15099);
#15101=PRESENTATION_STYLE_ASSIGNMENT((#15100));
ENDSEC;
END-ISO-10303-21;
